ISO-10303-21;
HEADER;
FILE_DESCRIPTION (('STEP AP214'),
    '1' );
FILE_NAME ('Turntable Bolt.step',
    '2026-10-09T10:51:02',
    ( '' ),
    ( '' ),
    'SwSTEP 2.0',
    'SolidWorks 2026',
    '' );
FILE_SCHEMA (( 'AUTOMOTIVE_DESIGN' ));
ENDSEC;

DATA;
#16=CARTESIAN_POINT ( 'NONE',  ( -9.107733615807006800, 37.00000000000000711, -96.06569921463757566 ) ) ;
#49=DIRECTION ( 'NONE',  ( -0.7944560844389300103, 0.000000000000000000, -0.6073216033519338586 ) ) ;
#79=ORIENTED_EDGE ( 'NONE', *, *, #13431, .F. ) ;
#215=ADVANCED_FACE ( 'NONE', ( #14014 ), #12056, .T. ) ;
#298=EDGE_LOOP ( 'NONE', ( #1646, #5855, #3036, #20103 ) ) ;
#321=AXIS2_PLACEMENT_3D ( 'NONE', #22086, #7878, #10397 ) ;
#347=CLOSED_SHELL ( 'NONE', ( #16015, #16676, #7875, #358, #5419, #11925, #2214, #215, #20046 ) ) ;
#358=ADVANCED_FACE ( 'NONE', ( #21968 ), #16637, .T. ) ;
#379=VERTEX_POINT ( 'NONE', #17766 ) ;
#526=FACE_OUTER_BOUND ( 'NONE', #19789, .T. ) ;
#749=SHAPE_REPRESENTATION_RELATIONSHIP ( 'NONE' , 'NONE' ,  #15634, #18406 ) ;
#941=AXIS2_PLACEMENT_3D ( 'NONE', #17592, #14035, #11967 ) ;
#1137=ORIENTED_EDGE ( 'NONE', *, *, #19027, .T. ) ;
#1245=EDGE_LOOP ( 'NONE', ( #20373, #14552, #1137, #6106 ) ) ;
#1361=FACE_OUTER_BOUND ( 'NONE', #2181, .T. ) ;
#1395=DIRECTION ( 'NONE',  ( 1.000000000000000000, 0.000000000000000000, 0.000000000000000000 ) ) ;
#1516=DIRECTION ( 'NONE',  ( -5.440186201345785633E-18, -1.000000000000000000, -1.334940939666367878E-17 ) ) ;
#1646=ORIENTED_EDGE ( 'NONE', *, *, #16659, .F. ) ;
#1672=DIRECTION ( 'NONE',  ( -5.440186201345785633E-18, -1.000000000000000000, -1.334940939666367878E-17 ) ) ;
#1778=SURFACE_STYLE_USAGE ( .BOTH. , #5432 ) ;
#2066=CARTESIAN_POINT ( 'NONE',  ( -1.163172771417702700, 30.00000000000000711, -89.99248318111824574 ) ) ;
#2181=EDGE_LOOP ( 'NONE', ( #3410, #6188, #11314, #6338 ) ) ;
#2214=ADVANCED_FACE ( 'NONE', ( #1361 ), #17099, .T. ) ;
#2336=CIRCLE ( 'NONE', #6376, 6.000000000000003553 ) ;
#2411=DIRECTION ( 'NONE',  ( -0.7944560844389302323, 1.242937374672305755E-17, -0.6073216033519337476 ) ) ;
#2464=( LENGTH_UNIT ( ) NAMED_UNIT ( * ) SI_UNIT ( .MILLI., .METRE. ) );
#2498=CIRCLE ( 'NONE', #6891, 9.999999999999998224 ) ;
#2728=PRODUCT_DEFINITION ( 'UNKNOWN', '', #15080, #16177 ) ;
#2990=LINE ( 'NONE', #22262, #3376 ) ;
#3036=ORIENTED_EDGE ( 'NONE', *, *, #5413, .T. ) ;
#3102=CARTESIAN_POINT ( 'NONE',  ( 0.000000000000000000, 0.000000000000000000, 0.000000000000000000 ) ) ;
#3193=CARTESIAN_POINT ( 'NONE',  ( -1.163172771417702700, 37.00000000000000711, -89.99248318111824574 ) ) ;
#3225=DIRECTION ( 'NONE',  ( 0.7944560844389294552, 0.000000000000000000, 0.6073216033519345247 ) ) ;
#3344=AXIS2_PLACEMENT_3D ( 'NONE', #5265, #10456, #6878 ) ;
#3376=VECTOR ( 'NONE', #5037, 1000.000000000000000 ) ;
#3409=DIRECTION ( 'NONE',  ( 5.440186201345785633E-18, 1.000000000000000000, 1.334940939666367878E-17 ) ) ;
#3410=ORIENTED_EDGE ( 'NONE', *, *, #17952, .F. ) ;
#3497=FILL_AREA_STYLE_COLOUR ( '', #13944 ) ;
#3594=EDGE_CURVE ( 'NONE', #10934, #4883, #2498, .T. ) ;
#3612=CARTESIAN_POINT ( 'NONE',  ( -1.163172771417702478, 87.00000000000001421, -89.99248318111824574 ) ) ;
#3645=CIRCLE ( 'NONE', #19420, 5.000000000000023981 ) ;
#3716=PRODUCT_DEFINITION_SHAPE ( 'NONE', 'NONE',  #2728 ) ;
#3773=DIRECTION ( 'NONE',  ( 5.440186201345785633E-18, 1.000000000000000000, 1.334940939666367878E-17 ) ) ;
#3892=DIRECTION ( 'NONE',  ( 5.440186201345810285E-18, 1.000000000000000000, 1.334940939666369727E-17 ) ) ;
#3990=FACE_OUTER_BOUND ( 'NONE', #15488, .T. ) ;
#4153=CYLINDRICAL_SURFACE ( 'NONE', #21321, 6.000000000000003553 ) ;
#4161=ORIENTED_EDGE ( 'NONE', *, *, #19027, .F. ) ;
#4306=AXIS2_PLACEMENT_3D ( 'NONE', #8694, #13892, #20999 ) ;
#4357=FACE_BOUND ( 'NONE', #16770, .T. ) ;
#4399=ORIENTED_EDGE ( 'NONE', *, *, #16149, .T. ) ;
#4425=ORIENTED_EDGE ( 'NONE', *, *, #9921, .F. ) ;
#4592=DIRECTION ( 'NONE',  ( -5.440186201345785633E-18, -1.000000000000000000, -1.334940939666367878E-17 ) ) ;
#4610=VERTEX_POINT ( 'NONE', #9534 ) ;
#4659=CARTESIAN_POINT ( 'NONE',  ( -1.163172771417702700, 37.00000000000000711, -89.99248318111824574 ) ) ;
#4800=FACE_OUTER_BOUND ( 'NONE', #22230, .T. ) ;
#4883=VERTEX_POINT ( 'NONE', #22334 ) ;
#4916=EDGE_CURVE ( 'NONE', #7484, #19228, #17214, .T. ) ;
#4930=CARTESIAN_POINT ( 'NONE',  ( -5.135453193612369738, 87.00000000000001421, -93.02909119787791781 ) ) ;
#4950=FACE_OUTER_BOUND ( 'NONE', #16362, .T. ) ;
#5037=DIRECTION ( 'NONE',  ( -5.440186201345785633E-18, -1.000000000000000000, -1.334940939666367878E-17 ) ) ;
#5127=STYLED_ITEM ( 'NONE', ( #19343 ), #17564 ) ;
#5256=CYLINDRICAL_SURFACE ( 'NONE', #19163, 9.999999999999998224 ) ;
#5265=CARTESIAN_POINT ( 'NONE',  ( -1.163172771417702700, 37.00000000000000711, -89.99248318111824574 ) ) ;
#5413=EDGE_CURVE ( 'NONE', #19228, #10934, #7933, .T. ) ;
#5419=ADVANCED_FACE ( 'NONE', ( #4357, #8276 ), #6336, .T. ) ;
#5429=CARTESIAN_POINT ( 'NONE',  ( -1.163172771417702478, 86.00000000000001421, -89.99248318111824574 ) ) ;
#5432=SURFACE_SIDE_STYLE ('',( #21178 ) ) ;
#5488=LINE ( 'NONE', #14145, #7700 ) ;
#5547=EDGE_CURVE ( 'NONE', #14225, #379, #5488, .T. ) ;
#5555=AXIS2_PLACEMENT_3D ( 'NONE', #14855, #7587, #14620 ) ;
#5757=FACE_OUTER_BOUND ( 'NONE', #1245, .T. ) ;
#5838=AXIS2_PLACEMENT_3D ( 'NONE', #4659, #3409, #11691 ) ;
#5855=ORIENTED_EDGE ( 'NONE', *, *, #16578, .F. ) ;
#6106=ORIENTED_EDGE ( 'NONE', *, *, #6858, .F. ) ;
#6188=ORIENTED_EDGE ( 'NONE', *, *, #13431, .T. ) ;
#6292=AXIS2_PLACEMENT_3D ( 'NONE', #3102, #12069, #1395 ) ;
#6320=CIRCLE ( 'NONE', #20241, 6.000000000000003553 ) ;
#6336=PLANE ( 'NONE',  #11363 ) ;
#6338=ORIENTED_EDGE ( 'NONE', *, *, #13322, .T. ) ;
#6376=AXIS2_PLACEMENT_3D ( 'NONE', #5429, #1672, #49 ) ;
#6450=DIRECTION ( 'NONE',  ( -0.7944560844389302323, 1.242937374672305755E-17, -0.6073216033519337476 ) ) ;
#6684=CARTESIAN_POINT ( 'NONE',  ( -1.163172771417702478, 87.00000000000001421, -89.99248318111824574 ) ) ;
#6830=EDGE_LOOP ( 'NONE', ( #16097, #8532 ) ) ;
#6858=EDGE_CURVE ( 'NONE', #379, #4610, #7089, .T. ) ;
#6878=DIRECTION ( 'NONE',  ( -0.7944560844389304544, 0.000000000000000000, -0.6073216033519334145 ) ) ;
#6891=AXIS2_PLACEMENT_3D ( 'NONE', #18409, #11062, #11178 ) ;
#7045=ORIENTED_EDGE ( 'NONE', *, *, #5413, .F. ) ;
#7062=CIRCLE ( 'NONE', #10388, 6.000000000000003553 ) ;
#7089=LINE ( 'NONE', #10202, #18415 ) ;
#7290=AXIS2_PLACEMENT_3D ( 'NONE', #22330, #11814, #8336 ) ;
#7484=VERTEX_POINT ( 'NONE', #16 ) ;
#7505=ORIENTED_EDGE ( 'NONE', *, *, #17396, .F. ) ;
#7587=DIRECTION ( 'NONE',  ( 5.440186201345785633E-18, 1.000000000000000000, 1.334940939666367878E-17 ) ) ;
#7700=VECTOR ( 'NONE', #21554, 1000.000000000000114 ) ;
#7751=DIRECTION ( 'NONE',  ( -0.5617652846616787432, -0.7071067811865489050, -0.4294412240912379164 ) ) ;
#7875=ADVANCED_FACE ( 'NONE', ( #4800 ), #5256, .T. ) ;
#7878=DIRECTION ( 'NONE',  ( -5.440186201345785633E-18, -1.000000000000000000, -1.334940939666367878E-17 ) ) ;
#7933=LINE ( 'NONE', #22033, #10633 ) ;
#8039=DIRECTION ( 'NONE',  ( 5.440186201345810285E-18, 1.000000000000000000, 1.334940939666369727E-17 ) ) ;
#8182=DIRECTION ( 'NONE',  ( 0.7944560844389300103, 0.000000000000000000, 0.6073216033519338586 ) ) ;
#8276=FACE_OUTER_BOUND ( 'NONE', #8644, .T. ) ;
#8336=DIRECTION ( 'NONE',  ( 0.7944560844389300103, 0.000000000000000000, 0.6073216033519338586 ) ) ;
#8470=VECTOR ( 'NONE', #20226, 1000.000000000000000 ) ;
#8532=ORIENTED_EDGE ( 'NONE', *, *, #9921, .T. ) ;
#8644=EDGE_LOOP ( 'NONE', ( #21791, #13796 ) ) ;
#8688=DIRECTION ( 'NONE',  ( -5.440186201345785633E-18, -1.000000000000000000, -1.334940939666367878E-17 ) ) ;
#8694=CARTESIAN_POINT ( 'NONE',  ( -1.163172771417702478, 87.00000000000001421, -89.99248318111824574 ) ) ;
#8755=( NAMED_UNIT ( * ) PLANE_ANGLE_UNIT ( ) SI_UNIT ( $, .RADIAN. ) );
#8977=ORIENTED_EDGE ( 'NONE', *, *, #21764, .F. ) ;
#9436=LINE ( 'NONE', #13251, #8470 ) ;
#9533=ORIENTED_EDGE ( 'NONE', *, *, #16659, .T. ) ;
#9534=CARTESIAN_POINT ( 'NONE',  ( 3.603563735215878250, 37.00000000000000711, -86.34855356100663926 ) ) ;
#9764=UNCERTAINTY_MEASURE_WITH_UNIT (LENGTH_MEASURE( 1.000000000000000082E-05 ), #15931, 'distance_accuracy_value', 'NONE');
#9921=EDGE_CURVE ( 'NONE', #11656, #14225, #18196, .T. ) ;
#10202=CARTESIAN_POINT ( 'NONE',  ( 3.603563735215880026, 87.00000000000001421, -86.34855356100663926 ) ) ;
#10340=CIRCLE ( 'NONE', #5555, 9.999999999999998224 ) ;
#10388=AXIS2_PLACEMENT_3D ( 'NONE', #12851, #3773, #11004 ) ;
#10397=DIRECTION ( 'NONE',  ( 0.7944560844389304544, 0.000000000000000000, 0.6073216033519334145 ) ) ;
#10456=DIRECTION ( 'NONE',  ( 5.440186201345785633E-18, 1.000000000000000000, 1.334940939666367878E-17 ) ) ;
#10462=ORIENTED_EDGE ( 'NONE', *, *, #5547, .F. ) ;
#10623=DIRECTION ( 'NONE',  ( 0.7944560844389294552, 0.000000000000000000, 0.6073216033519345247 ) ) ;
#10633=VECTOR ( 'NONE', #4592, 1000.000000000000000 ) ;
#10675=CONICAL_SURFACE ( 'NONE', #20564, 5.000000000000023981, 0.7853981633974460586 ) ;
#10814=AXIS2_PLACEMENT_3D ( 'NONE', #2066, #3892, #2411 ) ;
#10934=VERTEX_POINT ( 'NONE', #20730 ) ;
#11004=DIRECTION ( 'NONE',  ( -0.7944560844389300103, 0.000000000000000000, -0.6073216033519338586 ) ) ;
#11062=DIRECTION ( 'NONE',  ( 5.440186201345785633E-18, 1.000000000000000000, 1.334940939666367878E-17 ) ) ;
#11096=CARTESIAN_POINT ( 'NONE',  ( 2.809107650776963450, 87.00000000000001421, -86.95587516435855946 ) ) ;
#11178=DIRECTION ( 'NONE',  ( -0.7944560844389304544, 0.000000000000000000, -0.6073216033519334145 ) ) ;
#11179=CARTESIAN_POINT ( 'NONE',  ( -1.163172771417702478, 87.00000000000001421, -89.99248318111824574 ) ) ;
#11314=ORIENTED_EDGE ( 'NONE', *, *, #6858, .T. ) ;
#11363=AXIS2_PLACEMENT_3D ( 'NONE', #18396, #8039, #6450 ) ;
#11380=MECHANICAL_DESIGN_GEOMETRIC_PRESENTATION_REPRESENTATION('',(#5127),#11744);
#11656=VERTEX_POINT ( 'NONE', #4930 ) ;
#11670=ORIENTED_EDGE ( 'NONE', *, *, #13322, .F. ) ;
#11691=DIRECTION ( 'NONE',  ( -0.7944560844389304544, 0.000000000000000000, -0.6073216033519334145 ) ) ;
#11744=( GEOMETRIC_REPRESENTATION_CONTEXT ( 3 ) GLOBAL_UNCERTAINTY_ASSIGNED_CONTEXT ( ( #9764 ) ) GLOBAL_UNIT_ASSIGNED_CONTEXT ( ( #15931, #8755, #14894 ) ) REPRESENTATION_CONTEXT ( 'NONE', 'WORKASPACE' ) );
#11814=DIRECTION ( 'NONE',  ( -5.440186201345785633E-18, -1.000000000000000000, -1.334940939666367878E-17 ) ) ;
#11828=VERTEX_POINT ( 'NONE', #12414 ) ;
#11845=DIRECTION ( 'NONE',  ( -5.440186201345785633E-18, -1.000000000000000000, -1.334940939666367878E-17 ) ) ;
#11890=ORIENTED_EDGE ( 'NONE', *, *, #3594, .F. ) ;
#11925=ADVANCED_FACE ( 'NONE', ( #3990 ), #17829, .F. ) ;
#11967=DIRECTION ( 'NONE',  ( -0.7944560844389294552, 0.000000000000000000, -0.6073216033519345247 ) ) ;
#12056=PLANE ( 'NONE',  #4306 ) ;
#12069=DIRECTION ( 'NONE',  ( 0.000000000000000000, 0.000000000000000000, 1.000000000000000000 ) ) ;
#12258=AXIS2_PLACEMENT_3D ( 'NONE', #16822, #13712, #3225 ) ;
#12354=ORIENTED_EDGE ( 'NONE', *, *, #16149, .F. ) ;
#12401=CARTESIAN_POINT ( 'NONE',  ( -1.163172771417702478, 86.00000000000001421, -89.99248318111824574 ) ) ;
#12414=CARTESIAN_POINT ( 'NONE',  ( -5.929909278051283650, 86.00000000000001421, -93.63641280122985222 ) ) ;
#12584=FILL_AREA_STYLE ('',( #3497 ) ) ;
#12851=CARTESIAN_POINT ( 'NONE',  ( -1.163172771417702700, 37.00000000000000711, -89.99248318111824574 ) ) ;
#12975=ORIENTED_EDGE ( 'NONE', *, *, #5547, .T. ) ;
#13251=CARTESIAN_POINT ( 'NONE',  ( -9.107733615807006800, 37.00000000000000711, -96.06569921463757566 ) ) ;
#13273=CIRCLE ( 'NONE', #3344, 9.999999999999998224 ) ;
#13322=EDGE_CURVE ( 'NONE', #4610, #16423, #15936, .T. ) ;
#13431=EDGE_CURVE ( 'NONE', #11828, #379, #2336, .T. ) ;
#13499=CARTESIAN_POINT ( 'NONE',  ( -5.929909278051283650, 37.00000000000000711, -93.63641280122985222 ) ) ;
#13624=VECTOR ( 'NONE', #7751, 1000.000000000000114 ) ;
#13700=ORIENTED_EDGE ( 'NONE', *, *, #14897, .F. ) ;
#13712=DIRECTION ( 'NONE',  ( -5.440186201345785633E-18, -1.000000000000000000, -1.334940939666367878E-17 ) ) ;
#13796=ORIENTED_EDGE ( 'NONE', *, *, #4916, .T. ) ;
#13892=DIRECTION ( 'NONE',  ( 5.440186201345810285E-18, 1.000000000000000000, 1.334940939666369727E-17 ) ) ;
#13944=COLOUR_RGB ( '', 0.08235294, 0.09019608, 0.10196078) ;
#14014=FACE_OUTER_BOUND ( 'NONE', #6830, .T. ) ;
#14035=DIRECTION ( 'NONE',  ( 5.440186201345785633E-18, 1.000000000000000000, 1.334940939666367878E-17 ) ) ;
#14089=CONICAL_SURFACE ( 'NONE', #12258, 5.000000000000023981, 0.7853981633974460586 ) ;
#14106=APPLICATION_CONTEXT ( 'automotive_design' ) ;
#14145=CARTESIAN_POINT ( 'NONE',  ( 2.809107650776963450, 87.00000000000001421, -86.95587516435855946 ) ) ;
#14225=VERTEX_POINT ( 'NONE', #11096 ) ;
#14552=ORIENTED_EDGE ( 'NONE', *, *, #17952, .T. ) ;
#14620=DIRECTION ( 'NONE',  ( -0.7944560844389304544, 0.000000000000000000, -0.6073216033519334145 ) ) ;
#14787=CARTESIAN_POINT ( 'NONE',  ( -5.135453193612369738, 87.00000000000001421, -93.02909119787791781 ) ) ;
#14847=SHAPE_DEFINITION_REPRESENTATION ( #3716, #15634 ) ;
#14855=CARTESIAN_POINT ( 'NONE',  ( -1.163172771417702700, 30.00000000000000711, -89.99248318111824574 ) ) ;
#14858=APPLICATION_CONTEXT ( 'automotive_design' ) ;
#14894=( NAMED_UNIT ( * ) SI_UNIT ( $, .STERADIAN. ) SOLID_ANGLE_UNIT ( ) );
#14897=EDGE_CURVE ( 'NONE', #379, #11828, #6320, .T. ) ;
#15080=PRODUCT_DEFINITION_FORMATION_WITH_SPECIFIED_SOURCE ( 'ANY', '', #15851, .NOT_KNOWN. ) ;
#15488=EDGE_LOOP ( 'NONE', ( #11890, #8977 ) ) ;
#15634=SHAPE_REPRESENTATION ( 'Turntable Bolt', ( #6292 ), #20590 ) ;
#15851=PRODUCT ( 'Turntable Bolt', 'Turntable Bolt', '', ( #16451 ) ) ;
#15931=( LENGTH_UNIT ( ) NAMED_UNIT ( * ) SI_UNIT ( .MILLI., .METRE. ) );
#15936=CIRCLE ( 'NONE', #18126, 6.000000000000003553 ) ;
#16015=ADVANCED_FACE ( 'NONE', ( #526 ), #10675, .T. ) ;
#16097=ORIENTED_EDGE ( 'NONE', *, *, #17396, .T. ) ;
#16149=EDGE_CURVE ( 'NONE', #11656, #11828, #17776, .T. ) ;
#16177=PRODUCT_DEFINITION_CONTEXT ( 'detailed design', #14858, 'design' ) ;
#16213=ORIENTED_EDGE ( 'NONE', *, *, #4916, .F. ) ;
#16362=EDGE_LOOP ( 'NONE', ( #12354, #7505, #12975, #79 ) ) ;
#16423=VERTEX_POINT ( 'NONE', #13499 ) ;
#16451=PRODUCT_CONTEXT ( 'NONE', #14106, 'mechanical' ) ;
#16578=EDGE_CURVE ( 'NONE', #19228, #7484, #13273, .T. ) ;
#16637=CYLINDRICAL_SURFACE ( 'NONE', #321, 9.999999999999998224 ) ;
#16659=EDGE_CURVE ( 'NONE', #7484, #4883, #9436, .T. ) ;
#16676=ADVANCED_FACE ( 'NONE', ( #5757 ), #4153, .T. ) ;
#16770=EDGE_LOOP ( 'NONE', ( #11670, #4161 ) ) ;
#16822=CARTESIAN_POINT ( 'NONE',  ( -1.163172771417702478, 87.00000000000001421, -89.99248318111824574 ) ) ;
#17052=DIRECTION ( 'NONE',  ( 5.440186201345785633E-18, 1.000000000000000000, 1.334940939666367878E-17 ) ) ;
#17099=CYLINDRICAL_SURFACE ( 'NONE', #7290, 6.000000000000003553 ) ;
#17207=DIRECTION ( 'NONE',  ( -5.440186201345785633E-18, -1.000000000000000000, -1.334940939666367878E-17 ) ) ;
#17214=CIRCLE ( 'NONE', #5838, 9.999999999999998224 ) ;
#17396=EDGE_CURVE ( 'NONE', #14225, #11656, #3645, .T. ) ;
#17564=MANIFOLD_SOLID_BREP ( 'Stock-MAS-425-1', #347 ) ;
#17592=CARTESIAN_POINT ( 'NONE',  ( -1.163172771417702478, 87.00000000000001421, -89.99248318111824574 ) ) ;
#17766=CARTESIAN_POINT ( 'NONE',  ( 3.603563735215878250, 86.00000000000001421, -86.34855356100663926 ) ) ;
#17776=LINE ( 'NONE', #14787, #13624 ) ;
#17829=PLANE ( 'NONE',  #10814 ) ;
#17952=EDGE_CURVE ( 'NONE', #11828, #16423, #2990, .T. ) ;
#18109=( NAMED_UNIT ( * ) PLANE_ANGLE_UNIT ( ) SI_UNIT ( $, .RADIAN. ) );
#18126=AXIS2_PLACEMENT_3D ( 'NONE', #21175, #19226, #22531 ) ;
#18196=CIRCLE ( 'NONE', #941, 5.000000000000023981 ) ;
#18396=CARTESIAN_POINT ( 'NONE',  ( -1.163172771417702700, 37.00000000000000711, -89.99248318111824574 ) ) ;
#18406=ADVANCED_BREP_SHAPE_REPRESENTATION ( '', ( #17564, #6292 ), #20590 ) ;
#18409=CARTESIAN_POINT ( 'NONE',  ( -1.163172771417702700, 30.00000000000000711, -89.99248318111824574 ) ) ;
#18415=VECTOR ( 'NONE', #17207, 1000.000000000000000 ) ;
#18581=CARTESIAN_POINT ( 'NONE',  ( 6.781388072971601844, 37.00000000000000711, -83.91926714759891581 ) ) ;
#18834=DIRECTION ( 'NONE',  ( 0.7944560844389304544, 0.000000000000000000, 0.6073216033519334145 ) ) ;
#19027=EDGE_CURVE ( 'NONE', #16423, #4610, #7062, .T. ) ;
#19037=DIRECTION ( 'NONE',  ( -0.7944560844389300103, 0.000000000000000000, -0.6073216033519338586 ) ) ;
#19100=UNCERTAINTY_MEASURE_WITH_UNIT (LENGTH_MEASURE( 1.000000000000000082E-05 ), #2464, 'distance_accuracy_value', 'NONE');
#19163=AXIS2_PLACEMENT_3D ( 'NONE', #3193, #11845, #18834 ) ;
#19226=DIRECTION ( 'NONE',  ( 5.440186201345785633E-18, 1.000000000000000000, 1.334940939666367878E-17 ) ) ;
#19228=VERTEX_POINT ( 'NONE', #18581 ) ;
#19343=PRESENTATION_STYLE_ASSIGNMENT (( #1778 ) ) ;
#19420=AXIS2_PLACEMENT_3D ( 'NONE', #6684, #17052, #20694 ) ;
#19789=EDGE_LOOP ( 'NONE', ( #4425, #4399, #13700, #10462 ) ) ;
#19983=ORIENTED_EDGE ( 'NONE', *, *, #21764, .T. ) ;
#20046=ADVANCED_FACE ( 'NONE', ( #4950 ), #14089, .T. ) ;
#20103=ORIENTED_EDGE ( 'NONE', *, *, #3594, .T. ) ;
#20226=DIRECTION ( 'NONE',  ( -5.440186201345785633E-18, -1.000000000000000000, -1.334940939666367878E-17 ) ) ;
#20241=AXIS2_PLACEMENT_3D ( 'NONE', #12401, #8688, #19037 ) ;
#20373=ORIENTED_EDGE ( 'NONE', *, *, #14897, .T. ) ;
#20564=AXIS2_PLACEMENT_3D ( 'NONE', #3612, #21297, #10623 ) ;
#20590=( GEOMETRIC_REPRESENTATION_CONTEXT ( 3 ) GLOBAL_UNCERTAINTY_ASSIGNED_CONTEXT ( ( #19100 ) ) GLOBAL_UNIT_ASSIGNED_CONTEXT ( ( #2464, #18109, #21841 ) ) REPRESENTATION_CONTEXT ( 'NONE', 'WORKASPACE' ) );
#20694=DIRECTION ( 'NONE',  ( -0.7944560844389294552, 0.000000000000000000, -0.6073216033519345247 ) ) ;
#20730=CARTESIAN_POINT ( 'NONE',  ( 6.781388072971601844, 30.00000000000000711, -83.91926714759891581 ) ) ;
#20999=DIRECTION ( 'NONE',  ( -0.7944560844389302323, 1.242937374672305755E-17, -0.6073216033519337476 ) ) ;
#21175=CARTESIAN_POINT ( 'NONE',  ( -1.163172771417702700, 37.00000000000000711, -89.99248318111824574 ) ) ;
#21178=SURFACE_STYLE_FILL_AREA ( #12584 ) ;
#21297=DIRECTION ( 'NONE',  ( -5.440186201345785633E-18, -1.000000000000000000, -1.334940939666367878E-17 ) ) ;
#21321=AXIS2_PLACEMENT_3D ( 'NONE', #11179, #1516, #8182 ) ;
#21554=DIRECTION ( 'NONE',  ( 0.5617652846616786322, -0.7071067811865489050, 0.4294412240912380274 ) ) ;
#21764=EDGE_CURVE ( 'NONE', #4883, #10934, #10340, .T. ) ;
#21791=ORIENTED_EDGE ( 'NONE', *, *, #16578, .T. ) ;
#21841=( NAMED_UNIT ( * ) SI_UNIT ( $, .STERADIAN. ) SOLID_ANGLE_UNIT ( ) );
#21968=FACE_OUTER_BOUND ( 'NONE', #298, .T. ) ;
#22033=CARTESIAN_POINT ( 'NONE',  ( 6.781388072971600067, 37.00000000000000711, -83.91926714759891581 ) ) ;
#22086=CARTESIAN_POINT ( 'NONE',  ( -1.163172771417702700, 37.00000000000000711, -89.99248318111824574 ) ) ;
#22230=EDGE_LOOP ( 'NONE', ( #16213, #9533, #19983, #7045 ) ) ;
#22262=CARTESIAN_POINT ( 'NONE',  ( -5.929909278051286314, 87.00000000000001421, -93.63641280122985222 ) ) ;
#22330=CARTESIAN_POINT ( 'NONE',  ( -1.163172771417702478, 87.00000000000001421, -89.99248318111824574 ) ) ;
#22334=CARTESIAN_POINT ( 'NONE',  ( -9.107733615807006800, 30.00000000000000711, -96.06569921463757566 ) ) ;
#22531=DIRECTION ( 'NONE',  ( -0.7944560844389300103, 0.000000000000000000, -0.6073216033519338586 ) ) ;
ENDSEC;
END-ISO-10303-21;
